ISO-10303-21;
HEADER;
/* Generated by software containing ST-Developer
 * from STEP Tools, Inc. (www.steptools.com) 
 */

FILE_DESCRIPTION(
/* description */ ('Four-bar parallelogram arm'),
/* implementation_level */ '2;1');

FILE_NAME(
/* name */ 'Pivot keeper (1).step',
/* time_stamp */ '2026-10-28T03:24:55-07:00',
/* author */ (''),
/* organization */ (''),
/* preprocessor_version */ 'ST-DEVELOPER v20.2',
/* originating_system */ 'Autodesk Translation Framework v15.17.0.0',
/* authorisation */ '');

FILE_SCHEMA (('AUTOMOTIVE_DESIGN { 1 0 10303 214 3 1 1 }'));
ENDSEC;

DATA;
#10=MECHANICAL_DESIGN_GEOMETRIC_PRESENTATION_REPRESENTATION('',(#635),#14512);
#535=SHAPE_REPRESENTATION_RELATIONSHIP('SRR','None',#14756,#585);
#585=ADVANCED_BREP_SHAPE_REPRESENTATION('',(#693),#14471);
#635=STYLED_ITEM('',(#15101),#693);
#693=MANIFOLD_SOLID_BREP('Body1',#7339);
#800=FACE_BOUND('',#1787,.T.);
#801=FACE_BOUND('',#1789,.T.);
#1059=PLANE('',#8148);
#1060=PLANE('',#8149);
#1299=FACE_OUTER_BOUND('',#1784,.T.);
#1300=FACE_OUTER_BOUND('',#1785,.T.);
#1301=FACE_OUTER_BOUND('',#1786,.T.);
#1302=FACE_OUTER_BOUND('',#1788,.T.);
#1784=EDGE_LOOP('',(#5378,#5379,#5380,#5381));
#1785=EDGE_LOOP('',(#5382,#5383,#5384,#5385));
#1786=EDGE_LOOP('',(#5386));
#1787=EDGE_LOOP('',(#5387));
#1788=EDGE_LOOP('',(#5388));
#1789=EDGE_LOOP('',(#5389));
#2417=LINE('',#11871,#2811);
#2418=LINE('',#11877,#2812);
#2811=VECTOR('',#9487,0.225);
#2812=VECTOR('',#9494,0.9);
#3190=CIRCLE('',#8143,0.225);
#3191=CIRCLE('',#8144,0.225);
#3192=CIRCLE('',#8146,0.9);
#3193=CIRCLE('',#8147,0.9);
#3675=VERTEX_POINT('',#11868);
#3676=VERTEX_POINT('',#11870);
#3677=VERTEX_POINT('',#11874);
#3678=VERTEX_POINT('',#11876);
#4320=EDGE_CURVE('',#3675,#3675,#3190,.T.);
#4321=EDGE_CURVE('',#3675,#3676,#2417,.T.);
#4322=EDGE_CURVE('',#3676,#3676,#3191,.T.);
#4323=EDGE_CURVE('',#3677,#3677,#3192,.T.);
#4324=EDGE_CURVE('',#3677,#3678,#2418,.T.);
#4325=EDGE_CURVE('',#3678,#3678,#3193,.T.);
#5378=ORIENTED_EDGE('',*,*,#4320,.F.);
#5379=ORIENTED_EDGE('',*,*,#4321,.T.);
#5380=ORIENTED_EDGE('',*,*,#4322,.T.);
#5381=ORIENTED_EDGE('',*,*,#4321,.F.);
#5382=ORIENTED_EDGE('',*,*,#4323,.F.);
#5383=ORIENTED_EDGE('',*,*,#4324,.T.);
#5384=ORIENTED_EDGE('',*,*,#4325,.T.);
#5385=ORIENTED_EDGE('',*,*,#4324,.F.);
#5386=ORIENTED_EDGE('',*,*,#4323,.T.);
#5387=ORIENTED_EDGE('',*,*,#4320,.T.);
#5388=ORIENTED_EDGE('',*,*,#4325,.F.);
#5389=ORIENTED_EDGE('',*,*,#4322,.F.);
#6759=CYLINDRICAL_SURFACE('',#8142,0.225);
#6760=CYLINDRICAL_SURFACE('',#8145,0.9);
#7004=ADVANCED_FACE('',(#1299),#6759,.F.);
#7005=ADVANCED_FACE('',(#1300),#6760,.T.);
#7006=ADVANCED_FACE('',(#1301,#800),#1059,.T.);
#7007=ADVANCED_FACE('',(#1302,#801),#1060,.F.);
#7339=CLOSED_SHELL('',(#7004,#7005,#7006,#7007));
#8141=AXIS2_PLACEMENT_3D('',#11866,#9481,#9482);
#8142=AXIS2_PLACEMENT_3D('',#11867,#9483,#9484);
#8143=AXIS2_PLACEMENT_3D('',#11869,#9485,#9486);
#8144=AXIS2_PLACEMENT_3D('',#11872,#9488,#9489);
#8145=AXIS2_PLACEMENT_3D('',#11873,#9490,#9491);
#8146=AXIS2_PLACEMENT_3D('',#11875,#9492,#9493);
#8147=AXIS2_PLACEMENT_3D('',#11878,#9495,#9496);
#8148=AXIS2_PLACEMENT_3D('',#11879,#9497,#9498);
#8149=AXIS2_PLACEMENT_3D('',#11880,#9499,#9500);
#9481=DIRECTION('axis',(0.,0.,1.));
#9482=DIRECTION('refdir',(1.,0.,0.));
#9483=DIRECTION('center_axis',(0.,1.,0.));
#9484=DIRECTION('ref_axis',(1.,0.,0.));
#9485=DIRECTION('center_axis',(0.,-1.,0.));
#9486=DIRECTION('ref_axis',(1.,0.,0.));
#9487=DIRECTION('',(0.,-1.,0.));
#9488=DIRECTION('center_axis',(0.,-1.,0.));
#9489=DIRECTION('ref_axis',(1.,0.,0.));
#9490=DIRECTION('center_axis',(0.,1.,0.));
#9491=DIRECTION('ref_axis',(1.,0.,0.));
#9492=DIRECTION('center_axis',(0.,1.,0.));
#9493=DIRECTION('ref_axis',(1.,0.,0.));
#9494=DIRECTION('',(0.,-1.,0.));
#9495=DIRECTION('center_axis',(0.,1.,0.));
#9496=DIRECTION('ref_axis',(1.,0.,0.));
#9497=DIRECTION('center_axis',(0.,1.,0.));
#9498=DIRECTION('ref_axis',(1.,0.,0.));
#9499=DIRECTION('center_axis',(0.,1.,0.));
#9500=DIRECTION('ref_axis',(1.,0.,0.));
#11866=CARTESIAN_POINT('',(0.,0.,0.));
#11867=CARTESIAN_POINT('Origin',(0.,-1.8,14.));
#11868=CARTESIAN_POINT('',(-0.225,-1.6,14.));
#11869=CARTESIAN_POINT('Origin',(0.,-1.6,14.));
#11870=CARTESIAN_POINT('',(-0.225,-1.8,14.));
#11871=CARTESIAN_POINT('',(-0.225,-1.8,14.));
#11872=CARTESIAN_POINT('Origin',(0.,-1.8,14.));
#11873=CARTESIAN_POINT('Origin',(0.,-1.8,14.));
#11874=CARTESIAN_POINT('',(-0.9,-1.6,14.));
#11875=CARTESIAN_POINT('Origin',(0.,-1.6,14.));
#11876=CARTESIAN_POINT('',(-0.9,-1.8,14.));
#11877=CARTESIAN_POINT('',(-0.9,-1.8,14.));
#11878=CARTESIAN_POINT('Origin',(0.,-1.8,14.));
#11879=CARTESIAN_POINT('Origin',(0.,-1.6,14.));
#11880=CARTESIAN_POINT('Origin',(0.,-1.8,14.));
#14414=UNCERTAINTY_MEASURE_WITH_UNIT(LENGTH_MEASURE(0.001),#14513,
'DISTANCE_ACCURACY_VALUE',
'Maximum model space distance between geometric entities at asserted c
onnectivities');
#14455=UNCERTAINTY_MEASURE_WITH_UNIT(LENGTH_MEASURE(0.001),#14513,
'DISTANCE_ACCURACY_VALUE',
'Maximum model space distance between geometric entities at asserted c
onnectivities');
#14471=(
GEOMETRIC_REPRESENTATION_CONTEXT(3)
GLOBAL_UNCERTAINTY_ASSIGNED_CONTEXT((#14414))
GLOBAL_UNIT_ASSIGNED_CONTEXT((#14513,#14515,#14516))
REPRESENTATION_CONTEXT('','3D')
);
#14512=(
GEOMETRIC_REPRESENTATION_CONTEXT(3)
GLOBAL_UNCERTAINTY_ASSIGNED_CONTEXT((#14455))
GLOBAL_UNIT_ASSIGNED_CONTEXT((#14513,#14515,#14516))
REPRESENTATION_CONTEXT('','3D')
);
#14513=(
LENGTH_UNIT()
NAMED_UNIT(*)
SI_UNIT(.CENTI.,.METRE.)
);
#14515=(
NAMED_UNIT(*)
PLANE_ANGLE_UNIT()
SI_UNIT($,.RADIAN.)
);
#14516=(
NAMED_UNIT(*)
SI_UNIT($,.STERADIAN.)
SOLID_ANGLE_UNIT()
);
#14532=SHAPE_DEFINITION_REPRESENTATION(#14588,#14756);
#14588=PRODUCT_DEFINITION_SHAPE('',$,#14813);
#14756=SHAPE_REPRESENTATION('',(#8141),#14471);
#14797=PRODUCT_DEFINITION_CONTEXT('part definition',#14967,'design');
#14813=PRODUCT_DEFINITION('Pivot keeper (1)','Pivot keeper (1)',#14869,#14797);
#14869=PRODUCT_DEFINITION_FORMATION('',$,#14984);
#14967=APPLICATION_CONTEXT(
'Core Data for Automotive Mechanical Design Process');
#14968=PRODUCT_CONTEXT('part definition',#14967,'mechanical');
#14984=PRODUCT('Pivot keeper (1)','Pivot keeper (1)','Pivot keeper (1)',(#14968));
#15095=COLOUR_RGB('Off White',0.89,0.88,0.83);
#15096=FILL_AREA_STYLE_COLOUR('',#15095);
#15097=FILL_AREA_STYLE('',(#15096));
#15098=SURFACE_STYLE_FILL_AREA(#15097);
#15099=SURFACE_SIDE_STYLE('',(#15098));
#15100=SURFACE_STYLE_USAGE(.BOTH.,#15099);
#15101=PRESENTATION_STYLE_ASSIGNMENT((#15100));
ENDSEC;
END-ISO-10303-21;
